ISO-10303-21;
HEADER;
/* Generated by software containing ST-Developer
 * from STEP Tools, Inc. (www.steptools.com) 
 */

FILE_DESCRIPTION(
/* description */ ('Bin tilter linkage'),
/* implementation_level */ '2;1');

FILE_NAME(
/* name */ 'M4 short cap screw (4).step',
/* time_stamp */ '2026-10-28T03:26:24-07:00',
/* author */ (''),
/* organization */ (''),
/* preprocessor_version */ 'ST-DEVELOPER v20.2',
/* originating_system */ 'Autodesk Translation Framework v15.17.0.0',
/* authorisation */ '');

FILE_SCHEMA (('AUTOMOTIVE_DESIGN { 1 0 10303 214 3 1 1 }'));
ENDSEC;

DATA;
#10=MECHANICAL_DESIGN_GEOMETRIC_PRESENTATION_REPRESENTATION('',(#899),#23728);
#687=SHAPE_REPRESENTATION_RELATIONSHIP('SRR','None',#24152,#793);
#793=ADVANCED_BREP_SHAPE_REPRESENTATION('',(#1012),#23652);
#899=STYLED_ITEM('',(#24772),#1012);
#1012=MANIFOLD_SOLID_BREP('Body1',#12430);
#1278=FACE_BOUND('',#3160,.T.);
#1637=PLANE('',#14326);
#1638=PLANE('',#14331);
#1639=PLANE('',#14334);
#2191=FACE_OUTER_BOUND('',#3159,.T.);
#2192=FACE_OUTER_BOUND('',#3161,.T.);
#2193=FACE_OUTER_BOUND('',#3162,.T.);
#2194=FACE_OUTER_BOUND('',#3163,.T.);
#2195=FACE_OUTER_BOUND('',#3164,.T.);
#3159=EDGE_LOOP('',(#9577));
#3160=EDGE_LOOP('',(#9578));
#3161=EDGE_LOOP('',(#9579,#9580,#9581,#9582));
#3162=EDGE_LOOP('',(#9583));
#3163=EDGE_LOOP('',(#9584,#9585,#9586,#9587));
#3164=EDGE_LOOP('',(#9588));
#4143=LINE('',#21097,#4818);
#4144=LINE('',#21101,#4819);
#4818=VECTOR('',#17078,0.35);
#4819=VECTOR('',#17083,0.2);
#5507=CIRCLE('',#14327,0.35);
#5508=CIRCLE('',#14328,0.2);
#5509=CIRCLE('',#14330,0.35);
#5510=CIRCLE('',#14333,0.2);
#6357=VERTEX_POINT('',#21090);
#6358=VERTEX_POINT('',#21092);
#6359=VERTEX_POINT('',#21095);
#6360=VERTEX_POINT('',#21100);
#7528=EDGE_CURVE('',#6357,#6357,#5507,.T.);
#7529=EDGE_CURVE('',#6358,#6358,#5508,.T.);
#7530=EDGE_CURVE('',#6359,#6359,#5509,.T.);
#7531=EDGE_CURVE('',#6359,#6357,#4143,.T.);
#7532=EDGE_CURVE('',#6358,#6360,#4144,.T.);
#7533=EDGE_CURVE('',#6360,#6360,#5510,.T.);
#9577=ORIENTED_EDGE('',*,*,#7528,.F.);
#9578=ORIENTED_EDGE('',*,*,#7529,.T.);
#9579=ORIENTED_EDGE('',*,*,#7530,.F.);
#9580=ORIENTED_EDGE('',*,*,#7531,.T.);
#9581=ORIENTED_EDGE('',*,*,#7528,.T.);
#9582=ORIENTED_EDGE('',*,*,#7531,.F.);
#9583=ORIENTED_EDGE('',*,*,#7530,.T.);
#9584=ORIENTED_EDGE('',*,*,#7529,.F.);
#9585=ORIENTED_EDGE('',*,*,#7532,.T.);
#9586=ORIENTED_EDGE('',*,*,#7533,.T.);
#9587=ORIENTED_EDGE('',*,*,#7532,.F.);
#9588=ORIENTED_EDGE('',*,*,#7533,.F.);
#11419=CYLINDRICAL_SURFACE('',#14329,0.35);
#11420=CYLINDRICAL_SURFACE('',#14332,0.2);
#11916=ADVANCED_FACE('',(#2191,#1278),#1637,.F.);
#11917=ADVANCED_FACE('',(#2192),#11419,.T.);
#11918=ADVANCED_FACE('',(#2193),#1638,.T.);
#11919=ADVANCED_FACE('',(#2194),#11420,.T.);
#11920=ADVANCED_FACE('',(#2195),#1639,.F.);
#12430=CLOSED_SHELL('',(#11916,#11917,#11918,#11919,#11920));
#14325=AXIS2_PLACEMENT_3D('',#21088,#17066,#17067);
#14326=AXIS2_PLACEMENT_3D('',#21089,#17068,#17069);
#14327=AXIS2_PLACEMENT_3D('',#21091,#17070,#17071);
#14328=AXIS2_PLACEMENT_3D('',#21093,#17072,#17073);
#14329=AXIS2_PLACEMENT_3D('',#21094,#17074,#17075);
#14330=AXIS2_PLACEMENT_3D('',#21096,#17076,#17077);
#14331=AXIS2_PLACEMENT_3D('',#21098,#17079,#17080);
#14332=AXIS2_PLACEMENT_3D('',#21099,#17081,#17082);
#14333=AXIS2_PLACEMENT_3D('',#21102,#17084,#17085);
#14334=AXIS2_PLACEMENT_3D('',#21103,#17086,#17087);
#17066=DIRECTION('axis',(0.,0.,1.));
#17067=DIRECTION('refdir',(1.,0.,0.));
#17068=DIRECTION('center_axis',(0.,1.,0.));
#17069=DIRECTION('ref_axis',(1.,0.,0.));
#17070=DIRECTION('center_axis',(0.,1.,0.));
#17071=DIRECTION('ref_axis',(1.,0.,0.));
#17072=DIRECTION('center_axis',(0.,1.,0.));
#17073=DIRECTION('ref_axis',(1.,0.,0.));
#17074=DIRECTION('center_axis',(0.,1.,0.));
#17075=DIRECTION('ref_axis',(1.,0.,0.));
#17076=DIRECTION('center_axis',(0.,1.,0.));
#17077=DIRECTION('ref_axis',(1.,0.,0.));
#17078=DIRECTION('',(0.,-1.,0.));
#17079=DIRECTION('center_axis',(0.,1.,0.));
#17080=DIRECTION('ref_axis',(1.,0.,0.));
#17081=DIRECTION('center_axis',(0.,1.,0.));
#17082=DIRECTION('ref_axis',(1.,0.,0.));
#17083=DIRECTION('',(0.,-1.,0.));
#17084=DIRECTION('center_axis',(0.,1.,0.));
#17085=DIRECTION('ref_axis',(1.,0.,0.));
#17086=DIRECTION('center_axis',(0.,1.,0.));
#17087=DIRECTION('ref_axis',(1.,0.,0.));
#21088=CARTESIAN_POINT('',(0.,0.,0.));
#21089=CARTESIAN_POINT('Origin',(1.30814754519511,0.8,16.3081475451951));
#21090=CARTESIAN_POINT('',(0.958147545195113,0.8,16.3081475451951));
#21091=CARTESIAN_POINT('Origin',(1.30814754519511,0.8,16.3081475451951));
#21092=CARTESIAN_POINT('',(1.10814754519511,0.8,16.3081475451951));
#21093=CARTESIAN_POINT('Origin',(1.30814754519511,0.8,16.3081475451951));
#21094=CARTESIAN_POINT('Origin',(1.30814754519511,0.8,16.3081475451951));
#21095=CARTESIAN_POINT('',(0.958147545195113,1.2,16.3081475451951));
#21096=CARTESIAN_POINT('Origin',(1.30814754519511,1.2,16.3081475451951));
#21097=CARTESIAN_POINT('',(0.958147545195113,0.8,16.3081475451951));
#21098=CARTESIAN_POINT('Origin',(1.30814754519511,1.2,16.3081475451951));
#21099=CARTESIAN_POINT('Origin',(1.30814754519511,0.1,16.3081475451951));
#21100=CARTESIAN_POINT('',(1.10814754519511,0.1,16.3081475451951));
#21101=CARTESIAN_POINT('',(1.10814754519511,0.1,16.3081475451951));
#21102=CARTESIAN_POINT('Origin',(1.30814754519511,0.1,16.3081475451951));
#21103=CARTESIAN_POINT('Origin',(1.30814754519511,0.1,16.3081475451951));
#23535=UNCERTAINTY_MEASURE_WITH_UNIT(LENGTH_MEASURE(0.001),#23729,
'DISTANCE_ACCURACY_VALUE',
'Maximum model space distance between geometric entities at asserted c
onnectivities');
#23611=UNCERTAINTY_MEASURE_WITH_UNIT(LENGTH_MEASURE(0.001),#23729,
'DISTANCE_ACCURACY_VALUE',
'Maximum model space distance between geometric entities at asserted c
onnectivities');
#23652=(
GEOMETRIC_REPRESENTATION_CONTEXT(3)
GLOBAL_UNCERTAINTY_ASSIGNED_CONTEXT((#23535))
GLOBAL_UNIT_ASSIGNED_CONTEXT((#23729,#23731,#23732))
REPRESENTATION_CONTEXT('','3D')
);
#23728=(
GEOMETRIC_REPRESENTATION_CONTEXT(3)
GLOBAL_UNCERTAINTY_ASSIGNED_CONTEXT((#23611))
GLOBAL_UNIT_ASSIGNED_CONTEXT((#23729,#23731,#23732))
REPRESENTATION_CONTEXT('','3D')
);
#23729=(
LENGTH_UNIT()
NAMED_UNIT(*)
SI_UNIT(.CENTI.,.METRE.)
);
#23731=(
NAMED_UNIT(*)
PLANE_ANGLE_UNIT()
SI_UNIT($,.RADIAN.)
);
#23732=(
NAMED_UNIT(*)
SI_UNIT($,.STERADIAN.)
SOLID_ANGLE_UNIT()
);
#23773=SHAPE_DEFINITION_REPRESENTATION(#23889,#24152);
#23889=PRODUCT_DEFINITION_SHAPE('',$,#24269);
#24152=SHAPE_REPRESENTATION('',(#14325),#23652);
#24228=PRODUCT_DEFINITION_CONTEXT('part definition',#24578,'design');
#24269=PRODUCT_DEFINITION('M4 short cap screw (4)',
'M4 short cap screw (4)',#24385,#24228);
#24385=PRODUCT_DEFINITION_FORMATION('',$,#24620);
#24578=APPLICATION_CONTEXT(
'Core Data for Automotive Mechanical Design Process');
#24579=PRODUCT_CONTEXT('part definition',#24578,'mechanical');
#24620=PRODUCT('M4 short cap screw (4)','M4 short cap screw (4)',
'M4 short cap screw (4)',(#24579));
#24766=COLOUR_RGB('Black',0.12,0.14,0.17);
#24767=FILL_AREA_STYLE_COLOUR('',#24766);
#24768=FILL_AREA_STYLE('',(#24767));
#24769=SURFACE_STYLE_FILL_AREA(#24768);
#24770=SURFACE_SIDE_STYLE('',(#24769));
#24771=SURFACE_STYLE_USAGE(.BOTH.,#24770);
#24772=PRESENTATION_STYLE_ASSIGNMENT((#24771));
ENDSEC;
END-ISO-10303-21;
